ISO-10303-21;
HEADER;
/* Generated by software containing ST-Developer
 * from STEP Tools, Inc. (www.steptools.com) 
 */

FILE_DESCRIPTION(
/* description */ (''),
/* implementation_level */ '2;1');

FILE_NAME(
/* name */ 'Ball.step',
/* time_stamp */ '2026-10-23T17:22:31+06:00',
/* author */ (''),
/* organization */ (''),
/* preprocessor_version */ 'ST-DEVELOPER v20.2',
/* originating_system */ 'Autodesk Translation Framework v15.15.0.0',
/* authorisation */ '');

FILE_SCHEMA (('AUTOMOTIVE_DESIGN { 1 0 10303 214 3 1 1 }'));
ENDSEC;

DATA;
#10=MECHANICAL_DESIGN_GEOMETRIC_PRESENTATION_REPRESENTATION('',(#84),#7315);
#52=SPHERICAL_SURFACE('',#3697,1.5);
#64=SHAPE_REPRESENTATION_RELATIONSHIP('SRR','None',#7360,#74);
#74=ADVANCED_BREP_SHAPE_REPRESENTATION('',(#94),#7312);
#84=STYLED_ITEM('',(#7431),#94);
#94=MANIFOLD_SOLID_BREP('Ball',#3221);
#902=FACE_OUTER_BOUND('',#1093,.T.);
#1093=EDGE_LOOP('',(#3008,#3009));
#1282=CIRCLE('',#3698,1.5);
#1598=VERTEX_POINT('',#7255);
#1599=VERTEX_POINT('',#7256);
#2070=EDGE_CURVE('',#1598,#1599,#1282,.T.);
#3008=ORIENTED_EDGE('',*,*,#2070,.T.);
#3009=ORIENTED_EDGE('',*,*,#2070,.F.);
#3206=ADVANCED_FACE('',(#902),#52,.T.);
#3221=CLOSED_SHELL('',(#3206));
#3696=AXIS2_PLACEMENT_3D('',#7253,#4603,#4604);
#3697=AXIS2_PLACEMENT_3D('',#7254,#4605,#4606);
#3698=AXIS2_PLACEMENT_3D('',#7257,#4607,#4608);
#4603=DIRECTION('axis',(0.,0.,1.));
#4604=DIRECTION('refdir',(1.,0.,0.));
#4605=DIRECTION('center_axis',(0.,0.,1.));
#4606=DIRECTION('ref_axis',(1.,0.,0.));
#4607=DIRECTION('center_axis',(1.22464679914735E-16,-1.,0.));
#4608=DIRECTION('ref_axis',(-1.,-1.22464679914735E-16,0.));
#7253=CARTESIAN_POINT('',(0.,0.,0.));
#7254=CARTESIAN_POINT('Origin',(-9.1,0.,0.));
#7255=CARTESIAN_POINT('',(-9.1,-1.12481983699639E-32,1.5));
#7256=CARTESIAN_POINT('',(-9.1,-1.12481983699639E-32,-1.5));
#7257=CARTESIAN_POINT('Origin',(-9.1,0.,0.));
#7300=UNCERTAINTY_MEASURE_WITH_UNIT(LENGTH_MEASURE(0.01),#7316,
'DISTANCE_ACCURACY_VALUE',
'Maximum model space distance between geometric entities at asserted c
onnectivities');
#7303=UNCERTAINTY_MEASURE_WITH_UNIT(LENGTH_MEASURE(0.01),#7316,
'DISTANCE_ACCURACY_VALUE',
'Maximum model space distance between geometric entities at asserted c
onnectivities');
#7312=(
GEOMETRIC_REPRESENTATION_CONTEXT(3)
GLOBAL_UNCERTAINTY_ASSIGNED_CONTEXT((#7300))
GLOBAL_UNIT_ASSIGNED_CONTEXT((#7316,#7318,#7319))
REPRESENTATION_CONTEXT('','3D')
);
#7315=(
GEOMETRIC_REPRESENTATION_CONTEXT(3)
GLOBAL_UNCERTAINTY_ASSIGNED_CONTEXT((#7303))
GLOBAL_UNIT_ASSIGNED_CONTEXT((#7316,#7318,#7319))
REPRESENTATION_CONTEXT('','3D')
);
#7316=(
LENGTH_UNIT()
NAMED_UNIT(*)
SI_UNIT(.MILLI.,.METRE.)
);
#7318=(
NAMED_UNIT(*)
PLANE_ANGLE_UNIT()
SI_UNIT($,.RADIAN.)
);
#7319=(
NAMED_UNIT(*)
SI_UNIT($,.STERADIAN.)
SOLID_ANGLE_UNIT()
);
#7328=SHAPE_DEFINITION_REPRESENTATION(#7339,#7360);
#7339=PRODUCT_DEFINITION_SHAPE('',$,#7372);
#7360=SHAPE_REPRESENTATION('',(#3696),#7312);
#7363=PRODUCT_DEFINITION_CONTEXT('part definition',#7398,'design');
#7372=PRODUCT_DEFINITION('Ball','Ball',#7383,#7363);
#7383=PRODUCT_DEFINITION_FORMATION('',$,#7408);
#7398=APPLICATION_CONTEXT(
'Core Data for Automotive Mechanical Design Process');
#7399=PRODUCT_CONTEXT('part definition',#7398,'mechanical');
#7408=PRODUCT('Ball','Ball',$,(#7399));
#7425=COLOUR_RGB('Light Blue',0.38,0.62,0.78);
#7426=FILL_AREA_STYLE_COLOUR('',#7425);
#7427=FILL_AREA_STYLE('',(#7426));
#7428=SURFACE_STYLE_FILL_AREA(#7427);
#7429=SURFACE_SIDE_STYLE('',(#7428));
#7430=SURFACE_STYLE_USAGE(.BOTH.,#7429);
#7431=PRESENTATION_STYLE_ASSIGNMENT((#7430));
ENDSEC;
END-ISO-10303-21;
